ISO-10303-21;
HEADER;
FILE_DESCRIPTION (('STEP AP214'),
    '1' );
FILE_NAME ('CIRCLIP DIN 471 - 25 × 1.2_GB_CONNECTING_PIECE_RING_RRA 25.step',
    '2026-10-08T09:53:37',
    ( '' ),
    ( '' ),
    'SwSTEP 2.0',
    'SolidWorks 2026',
    '' );
FILE_SCHEMA (( 'AUTOMOTIVE_DESIGN' ));
ENDSEC;

DATA;
#15=DIRECTION ( 'NONE',  ( 9.814797785686868941E-17, -1.000000000000000000, 0.000000000000000000 ) ) ;
#107=DIRECTION ( 'NONE',  ( 9.814797785686868941E-17, 1.000000000000000000, -0.000000000000000000 ) ) ;
#174=CARTESIAN_POINT ( 'NONE',  ( -7.543218489614351263, -11.91259227951415056, -1.199999999999999956 ) ) ;
#185=VERTEX_POINT ( 'NONE', #57079 ) ;
#355=AXIS2_PLACEMENT_3D ( 'NONE', #45789, #68711, #63083 ) ;
#445=ORIENTED_EDGE ( 'NONE', *, *, #4200, .T. ) ;
#582=CARTESIAN_POINT ( 'NONE',  ( 1.250000000000000444, -16.78109714094927085, 0.000000000000000000 ) ) ;
#601=FACE_BOUND ( 'NONE', #61690, .T. ) ;
#833=CIRCLE ( 'NONE', #22361, 1.000000000000000888 ) ;
#834=CIRCLE ( 'NONE', #65457, 16.00000000000000000 ) ;
#944=PLANE ( 'NONE',  #67284 ) ;
#956=EDGE_CURVE ( 'NONE', #64091, #36317, #28160, .T. ) ;
#959=EDGE_CURVE ( 'NONE', #14859, #14793, #52027, .T. ) ;
#1046=ORIENTED_EDGE ( 'NONE', *, *, #53499, .F. ) ;
#1065=FILL_AREA_STYLE_COLOUR ( '', #49528 ) ;
#1090=CARTESIAN_POINT ( 'NONE',  ( 6.719258119307965238, -15.35072898742050107, 0.000000000000000000 ) ) ;
#1111=PRESENTATION_STYLE_ASSIGNMENT (( #54051 ) ) ;
#1193=AXIS2_PLACEMENT_3D ( 'NONE', #174, #70007, #57649 ) ;
#1243=DIRECTION ( 'NONE',  ( 0.000000000000000000, 0.000000000000000000, 1.000000000000000000 ) ) ;
#1304=DIRECTION ( 'NONE',  ( 0.000000000000000000, 0.000000000000000000, 1.000000000000000000 ) ) ;
#1339=EDGE_LOOP ( 'NONE', ( #20708, #25966, #12886, #8431 ) ) ;
#1467=CARTESIAN_POINT ( 'NONE',  ( 8.452893869119503023, -12.51233732111638375, -1.199999999999999956 ) ) ;
#1477=FILL_AREA_STYLE ('',( #48034 ) ) ;
#1493=DIRECTION ( 'NONE',  ( 0.000000000000000000, 0.000000000000000000, 1.000000000000000000 ) ) ;
#1505=AXIS2_PLACEMENT_3D ( 'NONE', #21389, #15770, #33046 ) ;
#1516=VERTEX_POINT ( 'NONE', #48238 ) ;
#1857=CARTESIAN_POINT ( 'NONE',  ( -1.250000000000000444, -16.78109714094927085, -1.199999999999999956 ) ) ;
#1858=VERTEX_POINT ( 'NONE', #51184 ) ;
#2025=EDGE_CURVE ( 'NONE', #36317, #26097, #34984, .T. ) ;
#2033=EDGE_CURVE ( 'NONE', #48200, #185, #64699, .T. ) ;
#2190=CARTESIAN_POINT ( 'NONE',  ( -11.59999999999999964, -0.8299999999999986278, 0.000000000000000000 ) ) ;
#2195=LINE ( 'NONE', #6685, #73174 ) ;
#2205=ORIENTED_EDGE ( 'NONE', *, *, #16288, .T. ) ;
#2314=DIRECTION ( 'NONE',  ( 0.000000000000000000, 0.000000000000000000, 1.000000000000000000 ) ) ;
#2373=CARTESIAN_POINT ( 'NONE',  ( 6.719258119307965238, -15.35072898742050107, -1.199999999999999956 ) ) ;
#2462=ORIENTED_EDGE ( 'NONE', *, *, #51771, .F. ) ;
#2648=DIRECTION ( 'NONE',  ( 0.000000000000000000, 0.000000000000000000, 1.000000000000000000 ) ) ;
#2669=DIRECTION ( 'NONE',  ( -1.000000000000000000, 0.000000000000000000, 0.000000000000000000 ) ) ;
#2677=CYLINDRICAL_SURFACE ( 'NONE', #16447, 16.00000000000000000 ) ;
#3025=VERTEX_POINT ( 'NONE', #51057 ) ;
#3127=AXIS2_PLACEMENT_3D ( 'NONE', #9089, #71491, #65882 ) ;
#3140=DIRECTION ( 'NONE',  ( 1.000000000000000000, 0.000000000000000000, 0.000000000000000000 ) ) ;
#3528=EDGE_CURVE ( 'NONE', #63719, #49170, #54172, .T. ) ;
#3764=VECTOR ( 'NONE', #14383, 1000.000000000000114 ) ;
#3768=DIRECTION ( 'NONE',  ( 0.000000000000000000, 0.000000000000000000, 1.000000000000000000 ) ) ;
#3790=EDGE_LOOP ( 'NONE', ( #65870, #31513, #9705, #21632 ) ) ;
#3919=DIRECTION ( 'NONE',  ( 0.000000000000000000, 0.000000000000000000, 1.000000000000000000 ) ) ;
#4200=EDGE_CURVE ( 'NONE', #11638, #64091, #65005, .T. ) ;
#4327=DIRECTION ( 'NONE',  ( 0.000000000000000000, 0.000000000000000000, 1.000000000000000000 ) ) ;
#4381=ORIENTED_EDGE ( 'NONE', *, *, #39501, .F. ) ;
#4578=ORIENTED_EDGE ( 'NONE', *, *, #42854, .T. ) ;
#4617=DIRECTION ( 'NONE',  ( 0.000000000000000000, 0.000000000000000000, 1.000000000000000000 ) ) ;
#4660=DIRECTION ( 'NONE',  ( 1.000000000000000000, 0.000000000000000000, 0.000000000000000000 ) ) ;
#4682=AXIS2_PLACEMENT_3D ( 'NONE', #52695, #1243, #25594 ) ;
#4896=CARTESIAN_POINT ( 'NONE',  ( -7.543218489614351263, -11.91259227951415056, 0.000000000000000000 ) ) ;
#5030=CYLINDRICAL_SURFACE ( 'NONE', #49971, 14.09999999999999964 ) ;
#5211=DIRECTION ( 'NONE',  ( 9.814797785686868941E-17, -1.000000000000000000, 0.000000000000000000 ) ) ;
#5259=CARTESIAN_POINT ( 'NONE',  ( 6.509281303079589520, -14.89695620656361008, 0.000000000000000000 ) ) ;
#5292=ORIENTED_EDGE ( 'NONE', *, *, #65095, .T. ) ;
#5343=LINE ( 'NONE', #17709, #14889 ) ;
#5348=DIRECTION ( 'NONE',  ( -0.000000000000000000, -0.000000000000000000, -1.000000000000000000 ) ) ;
#5501=DIRECTION ( 'NONE',  ( 0.000000000000000000, 0.000000000000000000, 1.000000000000000000 ) ) ;
#5620=DIRECTION ( 'NONE',  ( -1.000000000000000000, -9.814797785686868941E-17, 0.000000000000000000 ) ) ;
#5703=DIRECTION ( 'NONE',  ( 1.000000000000000000, 0.000000000000000000, 0.000000000000000000 ) ) ;
#5727=EDGE_CURVE ( 'NONE', #71661, #63816, #833, .T. ) ;
#5790=ORIENTED_EDGE ( 'NONE', *, *, #56082, .F. ) ;
#5816=VERTEX_POINT ( 'NONE', #45924 ) ;
#5995=ADVANCED_FACE ( 'NONE', ( #13168 ), #2677, .T. ) ;
#6119=EDGE_LOOP ( 'NONE', ( #36901, #50843, #16812, #55753 ) ) ;
#6183=VECTOR ( 'NONE', #53050, 1000.000000000000000 ) ;
#6331=ADVANCED_FACE ( 'NONE', ( #51457 ), #57116, .T. ) ;
#6532=AXIS2_PLACEMENT_3D ( 'NONE', #15588, #4327, #61460 ) ;
#6551=FACE_OUTER_BOUND ( 'NONE', #26793, .T. ) ;
#6587=CYLINDRICAL_SURFACE ( 'NONE', #41962, 14.09999999999999964 ) ;
#6646=ORIENTED_EDGE ( 'NONE', *, *, #2025, .T. ) ;
#6685=CARTESIAN_POINT ( 'NONE',  ( -11.59999999999999964, -0.8299999999999986278, -1.199999999999999956 ) ) ;
#6750=DIRECTION ( 'NONE',  ( -0.000000000000000000, -0.000000000000000000, -1.000000000000000000 ) ) ;
#6787=CIRCLE ( 'NONE', #11549, 14.09999999999999964 ) ;
#6941=FACE_OUTER_BOUND ( 'NONE', #22281, .T. ) ;
#7120=DIRECTION ( 'NONE',  ( -1.000000000000000000, 0.000000000000000000, 0.000000000000000000 ) ) ;
#7351=VECTOR ( 'NONE', #22916, 1000.000000000000000 ) ;
#7473=EDGE_LOOP ( 'NONE', ( #72656, #46595, #46048, #10734 ) ) ;
#7500=ADVANCED_FACE ( 'NONE', ( #64956 ), #52926, .F. ) ;
#7537=DIRECTION ( 'NONE',  ( 1.000000000000000000, 0.000000000000000000, 0.000000000000000000 ) ) ;
#7632=LINE ( 'NONE', #64789, #16569 ) ;
#7656=EDGE_CURVE ( 'NONE', #10101, #14764, #26564, .T. ) ;
#7822=DIRECTION ( 'NONE',  ( 0.000000000000000000, 0.000000000000000000, 1.000000000000000000 ) ) ;
#8046=CARTESIAN_POINT ( 'NONE',  ( 0.000000000000000000, -0.8299999999999999600, -1.199999999999999956 ) ) ;
#8177=DIRECTION ( 'NONE',  ( 1.000000000000000000, 0.000000000000000000, 0.000000000000000000 ) ) ;
#8379=LINE ( 'NONE', #4896, #3764 ) ;
#8428=DIRECTION ( 'NONE',  ( 1.000000000000000000, 0.000000000000000000, 0.000000000000000000 ) ) ;
#8431=ORIENTED_EDGE ( 'NONE', *, *, #57077, .F. ) ;
#8546=CYLINDRICAL_SURFACE ( 'NONE', #38407, 1.000000000000000000 ) ;
#8699=( GEOMETRIC_REPRESENTATION_CONTEXT ( 3 ) GLOBAL_UNCERTAINTY_ASSIGNED_CONTEXT ( ( #37041 ) ) GLOBAL_UNIT_ASSIGNED_CONTEXT ( ( #49095, #31796, #65298 ) ) REPRESENTATION_CONTEXT ( 'NONE', 'WORKASPACE' ) );
#8788=ORIENTED_EDGE ( 'NONE', *, *, #13832, .T. ) ;
#8834=VECTOR ( 'NONE', #33048, 1000.000000000000000 ) ;
#8888=ORIENTED_EDGE ( 'NONE', *, *, #51771, .T. ) ;
#8900=ADVANCED_FACE ( 'NONE', ( #64231 ), #47304, .F. ) ;
#8923=LINE ( 'NONE', #31841, #26855 ) ;
#9013=CARTESIAN_POINT ( 'NONE',  ( 0.000000000000000000, -0.8299999999999999600, -1.199999999999999956 ) ) ;
#9050=AXIS2_PLACEMENT_3D ( 'NONE', #74206, #46381, #39638 ) ;
#9089=CARTESIAN_POINT ( 'NONE',  ( 7.543218489614351263, -11.91259227951415056, -1.199999999999999956 ) ) ;
#9213=LINE ( 'NONE', #55077, #36564 ) ;
#9280=ORIENTED_EDGE ( 'NONE', *, *, #42140, .T. ) ;
#9450=AXIS2_PLACEMENT_3D ( 'NONE', #46061, #69722, #29484 ) ;
#9507=CARTESIAN_POINT ( 'NONE',  ( -4.250000000000000000, -13.95926121303099343, -1.199999999999999956 ) ) ;
#9539=CARTESIAN_POINT ( 'NONE',  ( 0.000000000000000000, 0.000000000000000000, -1.199999999999999956 ) ) ;
#9577=DIRECTION ( 'NONE',  ( 0.000000000000000000, 0.000000000000000000, 1.000000000000000000 ) ) ;
#9705=ORIENTED_EDGE ( 'NONE', *, *, #21968, .F. ) ;
#9734=EDGE_CURVE ( 'NONE', #20087, #49658, #39280, .T. ) ;
#9804=VERTEX_POINT ( 'NONE', #35839 ) ;
#9882=ORIENTED_EDGE ( 'NONE', *, *, #30822, .T. ) ;
#10045=SHAPE_REPRESENTATION ( 'CIRCLIP DIN 471 - 25 \X2\00d7\X0\ 1.2_GB_CONNECTING_PIECE_RING_RRA 25', ( #43395 ), #32718 ) ;
#10101=VERTEX_POINT ( 'NONE', #71392 ) ;
#10231=LINE ( 'NONE', #26774, #11980 ) ;
#10532=EDGE_CURVE ( 'NONE', #5816, #49658, #33557, .T. ) ;
#10671=DIRECTION ( 'NONE',  ( 1.000000000000000000, -9.814797785686868941E-17, 0.000000000000000000 ) ) ;
#10685=CYLINDRICAL_SURFACE ( 'NONE', #6532, 1.000000000000000888 ) ;
#10700=AXIS2_PLACEMENT_3D ( 'NONE', #9013, #3768, #32672 ) ;
#10734=ORIENTED_EDGE ( 'NONE', *, *, #49989, .F. ) ;
#11105=ADVANCED_FACE ( 'NONE', ( #60070 ), #8546, .F. ) ;
#11203=VERTEX_POINT ( 'NONE', #28794 ) ;
#11286=VECTOR ( 'NONE', #38154, 1000.000000000000000 ) ;
#11377=AXIS2_PLACEMENT_3D ( 'NONE', #21639, #33279, #22388 ) ;
#11549=AXIS2_PLACEMENT_3D ( 'NONE', #15547, #56141, #4660 ) ;
#11627=ORIENTED_EDGE ( 'NONE', *, *, #35030, .F. ) ;
#11638=VERTEX_POINT ( 'NONE', #12057 ) ;
#11719=VECTOR ( 'NONE', #32154, 1000.000000000000000 ) ;
#11791=CARTESIAN_POINT ( 'NONE',  ( 5.250000000000000000, -13.95926121303099343, -1.199999999999999956 ) ) ;
#11980=VECTOR ( 'NONE', #16249, 1000.000000000000000 ) ;
#12057=CARTESIAN_POINT ( 'NONE',  ( -11.59999999999999964, -0.8299999999999986278, -1.199999999999999956 ) ) ;
#12168=MANIFOLD_SOLID_BREP ( 'Fillet2', #72805 ) ;
#12180=EDGE_LOOP ( 'NONE', ( #40819, #8888, #42795, #20428 ) ) ;
#12204=AXIS2_PLACEMENT_3D ( 'NONE', #51710, #40058, #27274 ) ;
#12584=CARTESIAN_POINT ( 'NONE',  ( 0.000000000000000000, 0.000000000000000000, -1.199999999999999956 ) ) ;
#12681=CARTESIAN_POINT ( 'NONE',  ( 7.468086116107294004, -12.33868914344945189, 0.000000000000000000 ) ) ;
#12703=DIRECTION ( 'NONE',  ( 0.000000000000000000, 0.000000000000000000, 1.000000000000000000 ) ) ;
#12821=ORIENTED_EDGE ( 'NONE', *, *, #67215, .F. ) ;
#12886=ORIENTED_EDGE ( 'NONE', *, *, #959, .F. ) ;
#12953=DIRECTION ( 'NONE',  ( -0.000000000000000000, -0.000000000000000000, -1.000000000000000000 ) ) ;
#13168=FACE_OUTER_BOUND ( 'NONE', #7473, .T. ) ;
#13410=ORIENTED_EDGE ( 'NONE', *, *, #3528, .T. ) ;
#13546=VECTOR ( 'NONE', #56750, 1000.000000000000114 ) ;
#13652=DIRECTION ( 'NONE',  ( -1.000000000000000000, 0.000000000000000000, 0.000000000000000000 ) ) ;
#13768=CARTESIAN_POINT ( 'NONE',  ( -1.250000000000000444, -16.78109714094927085, 0.000000000000000000 ) ) ;
#13803=SURFACE_STYLE_FILL_AREA ( #1477 ) ;
#13832=EDGE_CURVE ( 'NONE', #32827, #54022, #50478, .T. ) ;
#13886=DIRECTION ( 'NONE',  ( 0.000000000000000000, 0.000000000000000000, 1.000000000000000000 ) ) ;
#14154=PRODUCT_DEFINITION ( 'UNKNOWN', '', #38807, #31111 ) ;
#14332=VECTOR ( 'NONE', #61019, 1000.000000000000000 ) ;
#14337=ORIENTED_EDGE ( 'NONE', *, *, #52262, .F. ) ;
#14357=DIRECTION ( 'NONE',  ( -0.000000000000000000, -0.000000000000000000, -1.000000000000000000 ) ) ;
#14383=DIRECTION ( 'NONE',  ( 0.1736481776669309418, -0.9848077530122080203, 0.000000000000000000 ) ) ;
#14393=CARTESIAN_POINT ( 'NONE',  ( -7.468086116107294004, -12.33868914344945189, -1.199999999999999956 ) ) ;
#14445=CARTESIAN_POINT ( 'NONE',  ( 14.09999999999999964, 0.000000000000000000, 0.000000000000000000 ) ) ;
#14675=CARTESIAN_POINT ( 'NONE',  ( 7.893099573151324044, -11.68370571044642503, 0.000000000000000000 ) ) ;
#14726=FACE_OUTER_BOUND ( 'NONE', #44858, .T. ) ;
#14764=VERTEX_POINT ( 'NONE', #12681 ) ;
#14793=VERTEX_POINT ( 'NONE', #40161 ) ;
#14859=VERTEX_POINT ( 'NONE', #1090 ) ;
#14889=VECTOR ( 'NONE', #107, 1000.000000000000000 ) ;
#15075=ORIENTED_EDGE ( 'NONE', *, *, #31320, .T. ) ;
#15141=ORIENTED_EDGE ( 'NONE', *, *, #60280, .T. ) ;
#15225=FACE_OUTER_BOUND ( 'NONE', #22176, .T. ) ;
#15328=ORIENTED_EDGE ( 'NONE', *, *, #51158, .F. ) ;
#15332=VERTEX_POINT ( 'NONE', #15887 ) ;
#15441=VERTEX_POINT ( 'NONE', #68332 ) ;
#15547=CARTESIAN_POINT ( 'NONE',  ( 0.000000000000000000, 0.000000000000000000, -1.199999999999999956 ) ) ;
#15587=AXIS2_PLACEMENT_3D ( 'NONE', #52282, #10671, #22330 ) ;
#15588=CARTESIAN_POINT ( 'NONE',  ( -4.250000000000000000, -13.95926121303099343, -1.199999999999999956 ) ) ;
#15609=ORIENTED_EDGE ( 'NONE', *, *, #35293, .T. ) ;
#15661=AXIS2_PLACEMENT_3D ( 'NONE', #5259, #33418, #46208 ) ;
#15770=DIRECTION ( 'NONE',  ( 0.000000000000000000, 0.000000000000000000, 1.000000000000000000 ) ) ;
#15887=CARTESIAN_POINT ( 'NONE',  ( -7.893099573151324044, -11.68370571044642503, -1.199999999999999956 ) ) ;
#15907=EDGE_LOOP ( 'NONE', ( #1046, #5292, #66135, #31627 ) ) ;
#16135=CARTESIAN_POINT ( 'NONE',  ( 5.250000000000000000, -13.95926121303099343, 0.000000000000000000 ) ) ;
#16249=DIRECTION ( 'NONE',  ( 0.000000000000000000, 0.000000000000000000, 1.000000000000000000 ) ) ;
#16276=DIRECTION ( 'NONE',  ( -0.000000000000000000, -0.000000000000000000, -1.000000000000000000 ) ) ;
#16280=SHAPE_DEFINITION_REPRESENTATION ( #27800, #10045 ) ;
#16288=EDGE_CURVE ( 'NONE', #9804, #56011, #18465, .T. ) ;
#16447=AXIS2_PLACEMENT_3D ( 'NONE', #19179, #43250, #7537 ) ;
#16555=EDGE_CURVE ( 'NONE', #48891, #20209, #60561, .T. ) ;
#16569=VECTOR ( 'NONE', #25302, 1000.000000000000000 ) ;
#16734=ORIENTED_EDGE ( 'NONE', *, *, #956, .F. ) ;
#16812=ORIENTED_EDGE ( 'NONE', *, *, #63180, .F. ) ;
#16910=CARTESIAN_POINT ( 'NONE',  ( -6.719258119307965238, -15.35072898742050107, 0.000000000000000000 ) ) ;
#17239=ORIENTED_EDGE ( 'NONE', *, *, #50674, .T. ) ;
#17296=AXIS2_PLACEMENT_3D ( 'NONE', #41694, #6750, #7120 ) ;
#17348=CARTESIAN_POINT ( 'NONE',  ( 0.000000000000000000, -0.8299999999999999600, 0.000000000000000000 ) ) ;
#17388=ORIENTED_EDGE ( 'NONE', *, *, #46335, .T. ) ;
#17519=CARTESIAN_POINT ( 'NONE',  ( 1.250000000000000000, -12.36245420541525597, -1.199999999999999956 ) ) ;
#17709=CARTESIAN_POINT ( 'NONE',  ( -1.250000000000000000, -12.36245420541525597, -1.199999999999999956 ) ) ;
#17735=ORIENTED_EDGE ( 'NONE', *, *, #40584, .F. ) ;
#17842=VECTOR ( 'NONE', #23465, 1000.000000000000000 ) ;
#17846=FACE_OUTER_BOUND ( 'NONE', #43383, .T. ) ;
#17856=FACE_OUTER_BOUND ( 'NONE', #43938, .T. ) ;
#17904=DIRECTION ( 'NONE',  ( 0.000000000000000000, 0.000000000000000000, 1.000000000000000000 ) ) ;
#17935=CIRCLE ( 'NONE', #20342, 16.00000000000000000 ) ;
#17941=DIRECTION ( 'NONE',  ( 1.000000000000000000, 0.000000000000000000, 0.000000000000000000 ) ) ;
#17950=ORIENTED_EDGE ( 'NONE', *, *, #22835, .F. ) ;
#17963=CIRCLE ( 'NONE', #60002, 1.000000000000000000 ) ;
#18017=ORIENTED_EDGE ( 'NONE', *, *, #5727, .T. ) ;
#18130=ORIENTED_EDGE ( 'NONE', *, *, #56958, .T. ) ;
#18247=ORIENTED_EDGE ( 'NONE', *, *, #35293, .F. ) ;
#18374=ORIENTED_EDGE ( 'NONE', *, *, #35627, .T. ) ;
#18465=CIRCLE ( 'NONE', #42477, 0.9999999999999991118 ) ;
#18678=ORIENTED_EDGE ( 'NONE', *, *, #68054, .F. ) ;
#18803=CARTESIAN_POINT ( 'NONE',  ( -3.249999999999999556, -13.95926121303099343, 0.000000000000000000 ) ) ;
#18837=ORIENTED_EDGE ( 'NONE', *, *, #68054, .T. ) ;
#18839=ORIENTED_EDGE ( 'NONE', *, *, #26976, .F. ) ;
#19098=LINE ( 'NONE', #41301, #28960 ) ;
#19179=CARTESIAN_POINT ( 'NONE',  ( 0.000000000000000000, -0.8299999999999999600, -1.199999999999999956 ) ) ;
#19328=CARTESIAN_POINT ( 'NONE',  ( 1.250000000000000000, -12.36245420541525597, 0.000000000000000000 ) ) ;
#19331=DIRECTION ( 'NONE',  ( 0.000000000000000000, 0.000000000000000000, 1.000000000000000000 ) ) ;
#19340=CARTESIAN_POINT ( 'NONE',  ( -14.09999999999999964, 1.726751986797767995E-15, -1.199999999999999956 ) ) ;
#19579=EDGE_LOOP ( 'NONE', ( #35247, #18678, #21199, #46077 ) ) ;
#19735=DIRECTION ( 'NONE',  ( 1.000000000000000000, 0.000000000000000000, 0.000000000000000000 ) ) ;
#20087=VERTEX_POINT ( 'NONE', #45625 ) ;
#20209=VERTEX_POINT ( 'NONE', #2373 ) ;
#20221=CIRCLE ( 'NONE', #53893, 1.000000000000000000 ) ;
#20342=AXIS2_PLACEMENT_3D ( 'NONE', #65353, #1493, #24379 ) ;
#20428=ORIENTED_EDGE ( 'NONE', *, *, #35255, .T. ) ;
#20620=VERTEX_POINT ( 'NONE', #66781 ) ;
#20635=DIRECTION ( 'NONE',  ( 1.000000000000000000, 0.000000000000000000, 0.000000000000000000 ) ) ;
#20704=CARTESIAN_POINT ( 'NONE',  ( -8.452893869119503023, -12.51233732111638375, 0.000000000000000000 ) ) ;
#20708=ORIENTED_EDGE ( 'NONE', *, *, #16555, .F. ) ;
#20765=CARTESIAN_POINT ( 'NONE',  ( 11.59999999999999964, -0.8299999999999999600, 0.000000000000000000 ) ) ;
#21199=ORIENTED_EDGE ( 'NONE', *, *, #9734, .T. ) ;
#21218=ORIENTED_EDGE ( 'NONE', *, *, #60127, .F. ) ;
#21351=AXIS2_PLACEMENT_3D ( 'NONE', #72798, #61182, #60810 ) ;
#21389=CARTESIAN_POINT ( 'NONE',  ( 0.000000000000000000, 0.000000000000000000, 0.000000000000000000 ) ) ;
#21536=CARTESIAN_POINT ( 'NONE',  ( 8.452893869119503023, -12.51233732111638375, 0.000000000000000000 ) ) ;
#21632=ORIENTED_EDGE ( 'NONE', *, *, #2033, .F. ) ;
#21639=CARTESIAN_POINT ( 'NONE',  ( -8.452893869119503023, -12.51233732111638375, -1.199999999999999956 ) ) ;
#21887=ORIENTED_EDGE ( 'NONE', *, *, #49989, .T. ) ;
#21968=EDGE_CURVE ( 'NONE', #185, #72505, #68614, .T. ) ;
#22085=VECTOR ( 'NONE', #2314, 1000.000000000000000 ) ;
#22141=DIRECTION ( 'NONE',  ( -1.000000000000000000, 0.000000000000000000, 0.000000000000000000 ) ) ;
#22176=EDGE_LOOP ( 'NONE', ( #16734, #36277, #30289, #36808 ) ) ;
#22281=EDGE_LOOP ( 'NONE', ( #65685, #67157, #27246, #17950 ) ) ;
#22330=DIRECTION ( 'NONE',  ( 9.814797785686868941E-17, 1.000000000000000000, 0.000000000000000000 ) ) ;
#22332=CARTESIAN_POINT ( 'NONE',  ( -14.09999999999999964, 1.726751986797767995E-15, -1.199999999999999956 ) ) ;
#22361=AXIS2_PLACEMENT_3D ( 'NONE', #46281, #29341, #5703 ) ;
#22388=DIRECTION ( 'NONE',  ( -1.000000000000000000, 0.000000000000000000, 0.000000000000000000 ) ) ;
#22641=VERTEX_POINT ( 'NONE', #18803 ) ;
#22660=VERTEX_POINT ( 'NONE', #48499 ) ;
#22835=EDGE_CURVE ( 'NONE', #3025, #9804, #32679, .T. ) ;
#22908=CARTESIAN_POINT ( 'NONE',  ( 7.543218489614351263, -11.91259227951415056, 0.000000000000000000 ) ) ;
#22910=DIRECTION ( 'NONE',  ( 1.000000000000000000, 0.000000000000000000, 0.000000000000000000 ) ) ;
#22916=DIRECTION ( 'NONE',  ( -0.000000000000000000, -0.000000000000000000, -1.000000000000000000 ) ) ;
#23138=PLANE ( 'NONE',  #9450 ) ;
#23189=DIRECTION ( 'NONE',  ( 1.000000000000000000, 0.000000000000000000, 0.000000000000000000 ) ) ;
#23273=FACE_OUTER_BOUND ( 'NONE', #51675, .T. ) ;
#23341=CARTESIAN_POINT ( 'NONE',  ( -5.250000000000000888, -13.95926121303099343, -1.199999999999999956 ) ) ;
#23361=VERTEX_POINT ( 'NONE', #582 ) ;
#23465=DIRECTION ( 'NONE',  ( 0.000000000000000000, 0.000000000000000000, 1.000000000000000000 ) ) ;
#23699=CARTESIAN_POINT ( 'NONE',  ( 14.09999999999999964, 0.000000000000000000, -1.199999999999999956 ) ) ;
#23749=CYLINDRICAL_SURFACE ( 'NONE', #4682, 11.59999999999999964 ) ;
#23808=CARTESIAN_POINT ( 'NONE',  ( 0.000000000000000000, -0.8299999999999999600, 0.000000000000000000 ) ) ;
#23898=VECTOR ( 'NONE', #62458, 1000.000000000000000 ) ;
#23957=ORIENTED_EDGE ( 'NONE', *, *, #54932, .F. ) ;
#23958=DIRECTION ( 'NONE',  ( 0.000000000000000000, 0.000000000000000000, 1.000000000000000000 ) ) ;
#23959=FILL_AREA_STYLE ('',( #1065 ) ) ;
#24003=( LENGTH_UNIT ( ) NAMED_UNIT ( * ) SI_UNIT ( .MILLI., .METRE. ) );
#24137=FACE_OUTER_BOUND ( 'NONE', #25414, .T. ) ;
#24242=ORIENTED_EDGE ( 'NONE', *, *, #956, .T. ) ;
#24251=DIRECTION ( 'NONE',  ( 0.000000000000000000, 0.000000000000000000, 1.000000000000000000 ) ) ;
#24356=DIRECTION ( 'NONE',  ( 1.000000000000000000, 0.000000000000000000, 0.000000000000000000 ) ) ;
#24379=DIRECTION ( 'NONE',  ( 1.000000000000000000, 0.000000000000000000, 0.000000000000000000 ) ) ;
#25071=AXIS2_PLACEMENT_3D ( 'NONE', #8046, #53918, #8428 ) ;
#25302=DIRECTION ( 'NONE',  ( 9.814797785686868941E-17, -1.000000000000000000, 0.000000000000000000 ) ) ;
#25320=VECTOR ( 'NONE', #52950, 1000.000000000000000 ) ;
#25414=EDGE_LOOP ( 'NONE', ( #52041, #445, #24242, #15328 ) ) ;
#25419=CIRCLE ( 'NONE', #12204, 14.09999999999999964 ) ;
#25594=DIRECTION ( 'NONE',  ( 1.000000000000000000, 0.000000000000000000, 0.000000000000000000 ) ) ;
#25644=PLANE ( 'NONE',  #3127 ) ;
#25861=EDGE_CURVE ( 'NONE', #1858, #15332, #55824, .T. ) ;
#25912=CARTESIAN_POINT ( 'NONE',  ( 4.250000000000000000, -13.95926121303099343, 0.000000000000000000 ) ) ;
#25966=ORIENTED_EDGE ( 'NONE', *, *, #35127, .F. ) ;
#26080=DIRECTION ( 'NONE',  ( -1.000000000000000000, 3.469446951953614189E-15, 0.000000000000000000 ) ) ;
#26097=VERTEX_POINT ( 'NONE', #19328 ) ;
#26270=CIRCLE ( 'NONE', #32277, 1.000000000000000888 ) ;
#26284=ADVANCED_FACE ( 'NONE', ( #44872 ), #5030, .T. ) ;
#26313=EDGE_CURVE ( 'NONE', #1516, #63719, #6787, .T. ) ;
#26470=FACE_OUTER_BOUND ( 'NONE', #64021, .T. ) ;
#26564=LINE ( 'NONE', #49498, #37733 ) ;
#26703=ORIENTED_EDGE ( 'NONE', *, *, #52266, .T. ) ;
#26745=ORIENTED_EDGE ( 'NONE', *, *, #16555, .T. ) ;
#26763=APPLICATION_CONTEXT ( 'automotive_design' ) ;
#26774=CARTESIAN_POINT ( 'NONE',  ( 3.250000000000000444, -13.95926121303099343, -1.199999999999999956 ) ) ;
#26793=EDGE_LOOP ( 'NONE', ( #18374, #17239, #72170, #2205, #32213, #57465, #9882, #36441, #41282, #29794, #6646, #32898, #53803, #28607, #32068, #47072 ) ) ;
#26855=VECTOR ( 'NONE', #48036, 1000.000000000000000 ) ;
#26976=EDGE_CURVE ( 'NONE', #11203, #32827, #70408, .T. ) ;
#27131=CARTESIAN_POINT ( 'NONE',  ( -4.250000000000000000, -13.95926121303099343, 0.000000000000000000 ) ) ;
#27246=ORIENTED_EDGE ( 'NONE', *, *, #39501, .T. ) ;
#27274=DIRECTION ( 'NONE',  ( 1.000000000000000000, 0.000000000000000000, 0.000000000000000000 ) ) ;
#27559=PRODUCT_CONTEXT ( 'NONE', #26763, 'mechanical' ) ;
#27583=EDGE_CURVE ( 'NONE', #70347, #20087, #60887, .T. ) ;
#27800=PRODUCT_DEFINITION_SHAPE ( 'NONE', 'NONE',  #14154 ) ;
#27835=EDGE_CURVE ( 'NONE', #49658, #5816, #28511, .T. ) ;
#28101=ORIENTED_EDGE ( 'NONE', *, *, #50674, .F. ) ;
#28160=LINE ( 'NONE', #50345, #8834 ) ;
#28223=VERTEX_POINT ( 'NONE', #56921 ) ;
#28237=AXIS2_PLACEMENT_3D ( 'NONE', #9507, #67771, #59255 ) ;
#28398=DIRECTION ( 'NONE',  ( 1.000000000000000000, 0.000000000000000000, 0.000000000000000000 ) ) ;
#28511=CIRCLE ( 'NONE', #70508, 1.000000000000000000 ) ;
#28607=ORIENTED_EDGE ( 'NONE', *, *, #959, .T. ) ;
#28755=ORIENTED_EDGE ( 'NONE', *, *, #29030, .F. ) ;
#28794=CARTESIAN_POINT ( 'NONE',  ( -6.719258119307965238, -15.35072898742050107, -1.199999999999999956 ) ) ;
#28960=VECTOR ( 'NONE', #7822, 1000.000000000000000 ) ;
#29030=EDGE_CURVE ( 'NONE', #28223, #20209, #71912, .T. ) ;
#29103=ADVANCED_FACE ( 'NONE', ( #23273 ), #33803, .T. ) ;
#29209=( LENGTH_UNIT ( ) NAMED_UNIT ( * ) SI_UNIT ( .MILLI., .METRE. ) );
#29263=LINE ( 'NONE', #34540, #7351 ) ;
#29341=DIRECTION ( 'NONE',  ( 0.000000000000000000, 0.000000000000000000, 1.000000000000000000 ) ) ;
#29368=ORIENTED_EDGE ( 'NONE', *, *, #71981, .F. ) ;
#29414=ADVANCED_FACE ( 'NONE', ( #48043 ), #70956, .T. ) ;
#29484=DIRECTION ( 'NONE',  ( -1.000000000000000000, 0.000000000000000000, 0.000000000000000000 ) ) ;
#29794=ORIENTED_EDGE ( 'NONE', *, *, #51158, .T. ) ;
#29888=DIRECTION ( 'NONE',  ( 0.000000000000000000, 0.000000000000000000, 1.000000000000000000 ) ) ;
#30099=DIRECTION ( 'NONE',  ( -0.000000000000000000, -0.000000000000000000, -1.000000000000000000 ) ) ;
#30289=ORIENTED_EDGE ( 'NONE', *, *, #67484, .T. ) ;
#30684=( NAMED_UNIT ( * ) PLANE_ANGLE_UNIT ( ) SI_UNIT ( $, .RADIAN. ) );
#30822=EDGE_CURVE ( 'NONE', #70837, #62740, #17935, .T. ) ;
#30947=ORIENTED_EDGE ( 'NONE', *, *, #26313, .T. ) ;
#30986=LINE ( 'NONE', #19340, #57130 ) ;
#31012=FACE_OUTER_BOUND ( 'NONE', #15907, .T. ) ;
#31053=VERTEX_POINT ( 'NONE', #14445 ) ;
#31100=SURFACE_SIDE_STYLE ('',( #13803 ) ) ;
#31111=PRODUCT_DEFINITION_CONTEXT ( 'detailed design', #48408, 'design' ) ;
#31254=ORIENTED_EDGE ( 'NONE', *, *, #5727, .F. ) ;
#31320=EDGE_CURVE ( 'NONE', #70347, #5816, #10231, .T. ) ;
#31427=CARTESIAN_POINT ( 'NONE',  ( -7.893099573151324044, -11.68370571044642503, -1.199999999999999956 ) ) ;
#31461=DIRECTION ( 'NONE',  ( 0.000000000000000000, 0.000000000000000000, 1.000000000000000000 ) ) ;
#31469=DIRECTION ( 'NONE',  ( 0.000000000000000000, 0.000000000000000000, 1.000000000000000000 ) ) ;
#31513=ORIENTED_EDGE ( 'NONE', *, *, #40778, .T. ) ;
#31627=ORIENTED_EDGE ( 'NONE', *, *, #41029, .F. ) ;
#31716=DIRECTION ( 'NONE',  ( 0.000000000000000000, 0.000000000000000000, 1.000000000000000000 ) ) ;
#31765=CARTESIAN_POINT ( 'NONE',  ( -6.719258119307966126, -15.35072898742050462, -1.199999999999999956 ) ) ;
#31767=CYLINDRICAL_SURFACE ( 'NONE', #61752, 11.59999999999999964 ) ;
#31796=( NAMED_UNIT ( * ) PLANE_ANGLE_UNIT ( ) SI_UNIT ( $, .RADIAN. ) );
#31841=CARTESIAN_POINT ( 'NONE',  ( 1.250000000000000444, -16.78109714094927085, -1.199999999999999956 ) ) ;
#31868=ORIENTED_EDGE ( 'NONE', *, *, #9734, .F. ) ;
#31972=ORIENTED_EDGE ( 'NONE', *, *, #16288, .F. ) ;
#32068=ORIENTED_EDGE ( 'NONE', *, *, #56082, .T. ) ;
#32141=MECHANICAL_DESIGN_GEOMETRIC_PRESENTATION_REPRESENTATION('',(#50121),#41761);
#32154=DIRECTION ( 'NONE',  ( 0.000000000000000000, 0.000000000000000000, 1.000000000000000000 ) ) ;
#32192=CARTESIAN_POINT ( 'NONE',  ( 4.250000000000000000, -13.95926121303099343, -1.199999999999999956 ) ) ;
#32213=ORIENTED_EDGE ( 'NONE', *, *, #35030, .T. ) ;
#32277=AXIS2_PLACEMENT_3D ( 'NONE', #27131, #55349, #3140 ) ;
#32285=ORIENTED_EDGE ( 'NONE', *, *, #42140, .F. ) ;
#32322=AXIS2_PLACEMENT_3D ( 'NONE', #25912, #43955, #55597 ) ;
#32345=DIRECTION ( 'NONE',  ( -0.000000000000000000, -0.000000000000000000, -1.000000000000000000 ) ) ;
#32407=ORIENTED_EDGE ( 'NONE', *, *, #53499, .T. ) ;
#32501=AXIS2_PLACEMENT_3D ( 'NONE', #43368, #36962, #66289 ) ;
#32511=DIRECTION ( 'NONE',  ( 1.000000000000000000, 0.000000000000000000, 0.000000000000000000 ) ) ;
#32672=DIRECTION ( 'NONE',  ( -1.000000000000000000, 0.000000000000000000, 0.000000000000000000 ) ) ;
#32679=CIRCLE ( 'NONE', #1505, 14.09999999999999964 ) ;
#32718=( GEOMETRIC_REPRESENTATION_CONTEXT ( 3 ) GLOBAL_UNCERTAINTY_ASSIGNED_CONTEXT ( ( #43455 ) ) GLOBAL_UNIT_ASSIGNED_CONTEXT ( ( #29209, #30684, #35231 ) ) REPRESENTATION_CONTEXT ( 'NONE', 'WORKASPACE' ) );
#32827=VERTEX_POINT ( 'NONE', #40305 ) ;
#32860=ADVANCED_FACE ( 'NONE', ( #24137 ), #23749, .F. ) ;
#32898=ORIENTED_EDGE ( 'NONE', *, *, #40584, .T. ) ;
#33046=DIRECTION ( 'NONE',  ( 1.000000000000000000, 0.000000000000000000, 0.000000000000000000 ) ) ;
#33048=DIRECTION ( 'NONE',  ( 0.000000000000000000, 0.000000000000000000, 1.000000000000000000 ) ) ;
#33096=EDGE_LOOP ( 'NONE', ( #11627, #43788, #9280, #8788 ) ) ;
#33279=DIRECTION ( 'NONE',  ( 0.000000000000000000, 0.000000000000000000, 1.000000000000000000 ) ) ;
#33386=ORIENTED_EDGE ( 'NONE', *, *, #25861, .F. ) ;
#33418=DIRECTION ( 'NONE',  ( 0.000000000000000000, 0.000000000000000000, 1.000000000000000000 ) ) ;
#33466=EDGE_LOOP ( 'NONE', ( #29368, #49493 ) ) ;
#33492=AXIS2_PLACEMENT_3D ( 'NONE', #39827, #39453, #22910 ) ;
#33523=LINE ( 'NONE', #45202, #34157 ) ;
#33557=CIRCLE ( 'NONE', #32322, 1.000000000000000000 ) ;
#33803=CYLINDRICAL_SURFACE ( 'NONE', #33492, 14.09999999999999964 ) ;
#33940=ORIENTED_EDGE ( 'NONE', *, *, #25861, .T. ) ;
#34057=CARTESIAN_POINT ( 'NONE',  ( -3.249999999999999556, -13.95926121303099343, -1.199999999999999956 ) ) ;
#34157=VECTOR ( 'NONE', #74124, 1000.000000000000114 ) ;
#34467=AXIS2_PLACEMENT_3D ( 'NONE', #53754, #13886, #2669 ) ;
#34476=FACE_OUTER_BOUND ( 'NONE', #70264, .T. ) ;
#34540=CARTESIAN_POINT ( 'NONE',  ( 7.001685179585692254, -14.98378029539707512, -1.199999999999999956 ) ) ;
#34624=AXIS2_PLACEMENT_3D ( 'NONE', #64187, #23958, #17941 ) ;
#34634=DIRECTION ( 'NONE',  ( 1.000000000000000000, 0.000000000000000000, 0.000000000000000000 ) ) ;
#34698=DIRECTION ( 'NONE',  ( -0.000000000000000000, -0.000000000000000000, -1.000000000000000000 ) ) ;
#34714=ADVANCED_FACE ( 'NONE', ( #40766, #63707, #6551 ), #944, .F. ) ;
#34725=CARTESIAN_POINT ( 'NONE',  ( 4.250000000000000000, -13.95926121303099343, -1.199999999999999956 ) ) ;
#34875=EDGE_CURVE ( 'NONE', #23361, #14859, #60107, .T. ) ;
#34927=AXIS2_PLACEMENT_3D ( 'NONE', #37405, #60702, #59211 ) ;
#34984=CIRCLE ( 'NONE', #38582, 11.59999999999999964 ) ;
#35030=EDGE_CURVE ( 'NONE', #56011, #54022, #8379, .T. ) ;
#35127=EDGE_CURVE ( 'NONE', #14793, #48891, #29263, .T. ) ;
#35231=( NAMED_UNIT ( * ) SI_UNIT ( $, .STERADIAN. ) SOLID_ANGLE_UNIT ( ) );
#35247=ORIENTED_EDGE ( 'NONE', *, *, #31320, .F. ) ;
#35255=EDGE_CURVE ( 'NONE', #22660, #62740, #54424, .T. ) ;
#35293=EDGE_CURVE ( 'NONE', #63719, #31053, #19098, .T. ) ;
#35386=DIRECTION ( 'NONE',  ( 1.000000000000000000, 0.000000000000000000, 0.000000000000000000 ) ) ;
#35448=ORIENTED_EDGE ( 'NONE', *, *, #27835, .F. ) ;
#35518=CYLINDRICAL_SURFACE ( 'NONE', #38068, 1.000000000000000888 ) ;
#35627=EDGE_CURVE ( 'NONE', #45615, #31053, #57785, .T. ) ;
#35839=CARTESIAN_POINT ( 'NONE',  ( -7.893099573151324044, -11.68370571044642503, 0.000000000000000000 ) ) ;
#35891=DIRECTION ( 'NONE',  ( 1.000000000000000000, 0.000000000000000000, 0.000000000000000000 ) ) ;
#36207=AXIS2_PLACEMENT_3D ( 'NONE', #58128, #17904, #23189 ) ;
#36277=ORIENTED_EDGE ( 'NONE', *, *, #60127, .T. ) ;
#36317=VERTEX_POINT ( 'NONE', #20765 ) ;
#36409=ORIENTED_EDGE ( 'NONE', *, *, #35127, .T. ) ;
#36441=ORIENTED_EDGE ( 'NONE', *, *, #55756, .T. ) ;
#36517=ORIENTED_EDGE ( 'NONE', *, *, #7656, .T. ) ;
#36564=VECTOR ( 'NONE', #56946, 1000.000000000000000 ) ;
#36615=FACE_OUTER_BOUND ( 'NONE', #3790, .T. ) ;
#36639=CYLINDRICAL_SURFACE ( 'NONE', #34927, 1.000000000000000000 ) ;
#36808=ORIENTED_EDGE ( 'NONE', *, *, #2025, .F. ) ;
#36901=ORIENTED_EDGE ( 'NONE', *, *, #46335, .F. ) ;
#36962=DIRECTION ( 'NONE',  ( 0.000000000000000000, 0.000000000000000000, 1.000000000000000000 ) ) ;
#36987=ORIENTED_EDGE ( 'NONE', *, *, #13832, .F. ) ;
#37041=UNCERTAINTY_MEASURE_WITH_UNIT (LENGTH_MEASURE( 1.000000000000000082E-05 ), #49095, 'distance_accuracy_value', 'NONE');
#37308=DIRECTION ( 'NONE',  ( 1.000000000000000000, 0.000000000000000000, 0.000000000000000000 ) ) ;
#37342=DIRECTION ( 'NONE',  ( 0.000000000000000000, 0.000000000000000000, -1.000000000000000000 ) ) ;
#37405=CARTESIAN_POINT ( 'NONE',  ( -8.452893869119503023, -12.51233732111638375, -1.199999999999999956 ) ) ;
#37708=CARTESIAN_POINT ( 'NONE',  ( 3.250000000000000444, -13.95926121303099343, -1.199999999999999956 ) ) ;
#37733=VECTOR ( 'NONE', #72424, 1000.000000000000000 ) ;
#38014=AXIS2_PLACEMENT_3D ( 'NONE', #51626, #34698, #41098 ) ;
#38068=AXIS2_PLACEMENT_3D ( 'NONE', #64469, #19331, #65214 ) ;
#38099=DIRECTION ( 'NONE',  ( -1.000000000000000000, 0.000000000000000000, 0.000000000000000000 ) ) ;
#38154=DIRECTION ( 'NONE',  ( -0.000000000000000000, -0.000000000000000000, -1.000000000000000000 ) ) ;
#38407=AXIS2_PLACEMENT_3D ( 'NONE', #32192, #31461, #71678 ) ;
#38582=AXIS2_PLACEMENT_3D ( 'NONE', #65808, #30099, #35386 ) ;
#38807=PRODUCT_DEFINITION_FORMATION_WITH_SPECIFIED_SOURCE ( 'ANY', '', #66185, .NOT_KNOWN. ) ;
#39280=LINE ( 'NONE', #11791, #17842 ) ;
#39339=DIRECTION ( 'NONE',  ( 0.000000000000000000, 0.000000000000000000, 1.000000000000000000 ) ) ;
#39453=DIRECTION ( 'NONE',  ( 0.000000000000000000, 0.000000000000000000, 1.000000000000000000 ) ) ;
#39501=EDGE_CURVE ( 'NONE', #15332, #9804, #49088, .T. ) ;
#39625=FACE_OUTER_BOUND ( 'NONE', #40808, .T. ) ;
#39638=DIRECTION ( 'NONE',  ( 1.000000000000000000, 0.000000000000000000, 0.000000000000000000 ) ) ;
#39827=CARTESIAN_POINT ( 'NONE',  ( 0.000000000000000000, 0.000000000000000000, -1.199999999999999956 ) ) ;
#40058=DIRECTION ( 'NONE',  ( 0.000000000000000000, 0.000000000000000000, 1.000000000000000000 ) ) ;
#40161=CARTESIAN_POINT ( 'NONE',  ( 7.001685179585692254, -14.98378029539707512, 0.000000000000000000 ) ) ;
#40305=CARTESIAN_POINT ( 'NONE',  ( -7.001685179585692254, -14.98378029539707512, -1.199999999999999956 ) ) ;
#40584=EDGE_CURVE ( 'NONE', #26097, #23361, #44685, .T. ) ;
#40614=ORIENTED_EDGE ( 'NONE', *, *, #27583, .T. ) ;
#40766=FACE_BOUND ( 'NONE', #67427, .T. ) ;
#40778=EDGE_CURVE ( 'NONE', #11638, #72505, #2195, .T. ) ;
#40808=EDGE_LOOP ( 'NONE', ( #67874, #48882, #18130, #51438 ) ) ;
#40819=ORIENTED_EDGE ( 'NONE', *, *, #30822, .F. ) ;
#40883=CYLINDRICAL_SURFACE ( 'NONE', #34624, 16.00000000000000000 ) ;
#41029=EDGE_CURVE ( 'NONE', #71661, #22641, #44615, .T. ) ;
#41098=DIRECTION ( 'NONE',  ( -1.000000000000000000, 0.000000000000000000, 0.000000000000000000 ) ) ;
#41234=CYLINDRICAL_SURFACE ( 'NONE', #355, 0.5000000000000004441 ) ;
#41282=ORIENTED_EDGE ( 'NONE', *, *, #21968, .T. ) ;
#41301=CARTESIAN_POINT ( 'NONE',  ( 14.09999999999999964, 0.000000000000000000, -1.199999999999999956 ) ) ;
#41694=CARTESIAN_POINT ( 'NONE',  ( 6.509281303079589520, -14.89695620656361008, -1.199999999999999956 ) ) ;
#41761=( GEOMETRIC_REPRESENTATION_CONTEXT ( 3 ) GLOBAL_UNCERTAINTY_ASSIGNED_CONTEXT ( ( #45886 ) ) GLOBAL_UNIT_ASSIGNED_CONTEXT ( ( #24003, #69846, #65701 ) ) REPRESENTATION_CONTEXT ( 'NONE', 'WORKASPACE' ) );
#41962=AXIS2_PLACEMENT_3D ( 'NONE', #12584, #24251, #58085 ) ;
#42025=DIRECTION ( 'NONE',  ( 0.000000000000000000, 0.000000000000000000, 1.000000000000000000 ) ) ;
#42036=CARTESIAN_POINT ( 'NONE',  ( 4.250000000000000000, -13.95926121303099343, -1.199999999999999956 ) ) ;
#42140=EDGE_CURVE ( 'NONE', #1858, #32827, #62288, .T. ) ;
#42477=AXIS2_PLACEMENT_3D ( 'NONE', #20704, #32345, #54548 ) ;
#42673=EDGE_CURVE ( 'NONE', #48200, #11638, #53438, .T. ) ;
#42795=ORIENTED_EDGE ( 'NONE', *, *, #67215, .T. ) ;
#42854=EDGE_CURVE ( 'NONE', #20620, #28223, #7632, .T. ) ;
#42979=LINE ( 'NONE', #14393, #59377 ) ;
#43246=CIRCLE ( 'NONE', #48053, 1.000000000000000888 ) ;
#43250=DIRECTION ( 'NONE',  ( 0.000000000000000000, 0.000000000000000000, 1.000000000000000000 ) ) ;
#43368=CARTESIAN_POINT ( 'NONE',  ( 0.000000000000000000, -0.8299999999999999600, 0.000000000000000000 ) ) ;
#43383=EDGE_LOOP ( 'NONE', ( #12821, #48885, #32285, #33940, #23957, #59730, #48724, #17388, #66594, #26745, #28755, #53349, #21218, #44244, #72550, #68621 ) ) ;
#43395=AXIS2_PLACEMENT_3D ( 'NONE', #48320, #71232, #19735 ) ;
#43399=AXIS2_PLACEMENT_3D ( 'NONE', #42036, #12703, #8177 ) ;
#43408=CARTESIAN_POINT ( 'NONE',  ( 8.452893869119503023, -12.51233732111638375, -1.199999999999999956 ) ) ;
#43455=UNCERTAINTY_MEASURE_WITH_UNIT (LENGTH_MEASURE( 1.000000000000000082E-05 ), #29209, 'distance_accuracy_value', 'NONE');
#43588=CARTESIAN_POINT ( 'NONE',  ( -4.250000000000000000, -13.95926121303099343, 0.000000000000000000 ) ) ;
#43788=ORIENTED_EDGE ( 'NONE', *, *, #52262, .T. ) ;
#43810=EDGE_CURVE ( 'NONE', #15441, #22641, #26270, .T. ) ;
#43938=EDGE_LOOP ( 'NONE', ( #74239, #31254, #67373, #64280 ) ) ;
#43955=DIRECTION ( 'NONE',  ( 0.000000000000000000, 0.000000000000000000, 1.000000000000000000 ) ) ;
#44174=CARTESIAN_POINT ( 'NONE',  ( 0.000000000000000000, -0.8299999999999999600, -1.199999999999999956 ) ) ;
#44244=ORIENTED_EDGE ( 'NONE', *, *, #4200, .F. ) ;
#44615=LINE ( 'NONE', #34057, #68422 ) ;
#44685=LINE ( 'NONE', #67602, #55147 ) ;
#44774=STYLED_ITEM ( 'NONE', ( #71649 ), #72270 ) ;
#44858=EDGE_LOOP ( 'NONE', ( #26703, #36517, #5790, #36409 ) ) ;
#44872=FACE_OUTER_BOUND ( 'NONE', #72304, .T. ) ;
#44997=DIRECTION ( 'NONE',  ( 0.1736481776669309418, -0.9848077530122080203, 0.000000000000000000 ) ) ;
#45202=CARTESIAN_POINT ( 'NONE',  ( 7.543218489614351263, -11.91259227951415056, -1.199999999999999956 ) ) ;
#45472=LINE ( 'NONE', #22908, #13546 ) ;
#45615=VERTEX_POINT ( 'NONE', #14675 ) ;
#45625=CARTESIAN_POINT ( 'NONE',  ( 5.250000000000000000, -13.95926121303099343, -1.199999999999999956 ) ) ;
#45789=CARTESIAN_POINT ( 'NONE',  ( -6.509281303079589520, -14.89695620656361008, -1.199999999999999956 ) ) ;
#45846=CARTESIAN_POINT ( 'NONE',  ( 1.250000000000000000, -12.36245420541525597, -1.199999999999999956 ) ) ;
#45886=UNCERTAINTY_MEASURE_WITH_UNIT (LENGTH_MEASURE( 1.000000000000000082E-05 ), #24003, 'distance_accuracy_value', 'NONE');
#45924=CARTESIAN_POINT ( 'NONE',  ( 3.250000000000000444, -13.95926121303099343, 0.000000000000000000 ) ) ;
#46048=ORIENTED_EDGE ( 'NONE', *, *, #34875, .F. ) ;
#46061=CARTESIAN_POINT ( 'NONE',  ( 0.000000000000000000, -0.8299999999999999600, -1.199999999999999956 ) ) ;
#46077=ORIENTED_EDGE ( 'NONE', *, *, #27835, .T. ) ;
#46081=CARTESIAN_POINT ( 'NONE',  ( 0.000000000000000000, -0.8299999999999999600, -1.199999999999999956 ) ) ;
#46180=ADVANCED_FACE ( 'NONE', ( #6941 ), #6587, .T. ) ;
#46208=DIRECTION ( 'NONE',  ( -1.000000000000000000, 3.469446951953611033E-15, 0.000000000000000000 ) ) ;
#46281=CARTESIAN_POINT ( 'NONE',  ( -4.250000000000000000, -13.95926121303099343, -1.199999999999999956 ) ) ;
#46335=EDGE_CURVE ( 'NONE', #1516, #10101, #17963, .T. ) ;
#46381=DIRECTION ( 'NONE',  ( -0.000000000000000000, -0.000000000000000000, -1.000000000000000000 ) ) ;
#46554=COLOUR_RGB ( '', 0.31764706, 0.68627451, 0.89019608) ;
#46595=ORIENTED_EDGE ( 'NONE', *, *, #57077, .T. ) ;
#46895=SURFACE_STYLE_FILL_AREA ( #23959 ) ;
#47072=ORIENTED_EDGE ( 'NONE', *, *, #63180, .T. ) ;
#47304=CYLINDRICAL_SURFACE ( 'NONE', #43399, 1.000000000000000000 ) ;
#47361=CIRCLE ( 'NONE', #66423, 11.59999999999999964 ) ;
#47483=DIRECTION ( 'NONE',  ( 1.000000000000000000, 0.000000000000000000, 0.000000000000000000 ) ) ;
#47578=CIRCLE ( 'NONE', #57193, 1.000000000000000000 ) ;
#47676=ADVANCED_FACE ( 'NONE', ( #26470 ), #36639, .F. ) ;
#47869=DIRECTION ( 'NONE',  ( -0.000000000000000000, 0.000000000000000000, -1.000000000000000000 ) ) ;
#47895=CARTESIAN_POINT ( 'NONE',  ( -7.001685179585692254, -14.98378029539707512, 0.000000000000000000 ) ) ;
#47999=SURFACE_SIDE_STYLE ('',( #46895 ) ) ;
#48032=DIRECTION ( 'NONE',  ( 1.000000000000000000, 0.000000000000000000, 0.000000000000000000 ) ) ;
#48034=FILL_AREA_STYLE_COLOUR ( '', #46554 ) ;
#48036=DIRECTION ( 'NONE',  ( 0.000000000000000000, 0.000000000000000000, 1.000000000000000000 ) ) ;
#48043=FACE_OUTER_BOUND ( 'NONE', #1339, .T. ) ;
#48053=AXIS2_PLACEMENT_3D ( 'NONE', #43588, #2648, #20635 ) ;
#48087=EDGE_LOOP ( 'NONE', ( #18837, #40614 ) ) ;
#48200=VERTEX_POINT ( 'NONE', #70752 ) ;
#48238=CARTESIAN_POINT ( 'NONE',  ( 7.893099573151324044, -11.68370571044642503, -1.199999999999999956 ) ) ;
#48320=CARTESIAN_POINT ( 'NONE',  ( 0.000000000000000000, 0.000000000000000000, 0.000000000000000000 ) ) ;
#48408=APPLICATION_CONTEXT ( 'automotive_design' ) ;
#48499=CARTESIAN_POINT ( 'NONE',  ( -1.250000000000000444, -16.78109714094927085, -1.199999999999999956 ) ) ;
#48724=ORIENTED_EDGE ( 'NONE', *, *, #26313, .F. ) ;
#48782=ADVANCED_FACE ( 'NONE', ( #34476 ), #41234, .T. ) ;
#48882=ORIENTED_EDGE ( 'NONE', *, *, #35255, .F. ) ;
#48885=ORIENTED_EDGE ( 'NONE', *, *, #26976, .T. ) ;
#48891=VERTEX_POINT ( 'NONE', #72011 ) ;
#49088=LINE ( 'NONE', #31427, #11719 ) ;
#49095=( LENGTH_UNIT ( ) NAMED_UNIT ( * ) SI_UNIT ( .MILLI., .METRE. ) );
#49136=CARTESIAN_POINT ( 'NONE',  ( 0.000000000000000000, -0.8299999999999999600, -1.199999999999999956 ) ) ;
#49170=VERTEX_POINT ( 'NONE', #22332 ) ;
#49493=ORIENTED_EDGE ( 'NONE', *, *, #43810, .F. ) ;
#49498=CARTESIAN_POINT ( 'NONE',  ( 7.468086116107294004, -12.33868914344945189, 0.000000000000000000 ) ) ;
#49528=COLOUR_RGB ( '', 0.31764706, 0.68627451, 0.89019608) ;
#49658=VERTEX_POINT ( 'NONE', #16135 ) ;
#49971=AXIS2_PLACEMENT_3D ( 'NONE', #9539, #3919, #61422 ) ;
#49989=EDGE_CURVE ( 'NONE', #28223, #23361, #8923, .T. ) ;
#50121=STYLED_ITEM ( 'NONE', ( #1111 ), #12168 ) ;
#50345=CARTESIAN_POINT ( 'NONE',  ( 11.59999999999999964, -0.8299999999999999600, -1.199999999999999956 ) ) ;
#50478=LINE ( 'NONE', #67021, #14332 ) ;
#50563=ADVANCED_FACE ( 'NONE', ( #31012 ), #10685, .F. ) ;
#50674=EDGE_CURVE ( 'NONE', #31053, #3025, #64122, .T. ) ;
#50763=MECHANICAL_DESIGN_GEOMETRIC_PRESENTATION_REPRESENTATION('',(#44774),#8699);
#50792=ORIENTED_EDGE ( 'NONE', *, *, #52417, .F. ) ;
#50843=ORIENTED_EDGE ( 'NONE', *, *, #57536, .F. ) ;
#50892=CARTESIAN_POINT ( 'NONE',  ( -3.249999999999999556, -13.95926121303099343, -1.199999999999999956 ) ) ;
#50906=DIRECTION ( 'NONE',  ( 1.000000000000000000, 0.000000000000000000, 0.000000000000000000 ) ) ;
#50944=CIRCLE ( 'NONE', #52124, 0.5000000000000004441 ) ;
#51057=CARTESIAN_POINT ( 'NONE',  ( -14.09999999999999964, 1.726751986797767995E-15, 0.000000000000000000 ) ) ;
#51158=EDGE_CURVE ( 'NONE', #72505, #36317, #47361, .T. ) ;
#51184=CARTESIAN_POINT ( 'NONE',  ( -7.468086116107294004, -12.33868914344945189, -1.199999999999999956 ) ) ;
#51190=DIRECTION ( 'NONE',  ( -1.000000000000000000, 0.000000000000000000, 0.000000000000000000 ) ) ;
#51438=ORIENTED_EDGE ( 'NONE', *, *, #2033, .T. ) ;
#51457=FACE_OUTER_BOUND ( 'NONE', #55542, .T. ) ;
#51626=CARTESIAN_POINT ( 'NONE',  ( -6.509281303079589520, -14.89695620656361008, -1.199999999999999956 ) ) ;
#51675=EDGE_LOOP ( 'NONE', ( #30947, #15609, #73335, #54546 ) ) ;
#51710=CARTESIAN_POINT ( 'NONE',  ( 0.000000000000000000, 0.000000000000000000, -1.199999999999999956 ) ) ;
#51771=EDGE_CURVE ( 'NONE', #70837, #11203, #66734, .T. ) ;
#52027=CIRCLE ( 'NONE', #15661, 0.5000000000000004441 ) ;
#52041=ORIENTED_EDGE ( 'NONE', *, *, #40778, .F. ) ;
#52058=FACE_BOUND ( 'NONE', #48087, .T. ) ;
#52124=AXIS2_PLACEMENT_3D ( 'NONE', #56101, #4617, #51190 ) ;
#52262=EDGE_CURVE ( 'NONE', #56011, #1858, #42979, .T. ) ;
#52266=EDGE_CURVE ( 'NONE', #48891, #10101, #33523, .T. ) ;
#52282=CARTESIAN_POINT ( 'NONE',  ( -1.250000000000000000, -12.36245420541525597, -1.199999999999999956 ) ) ;
#52417=EDGE_CURVE ( 'NONE', #54022, #70837, #50944, .T. ) ;
#52695=CARTESIAN_POINT ( 'NONE',  ( 0.000000000000000000, -0.8299999999999999600, -1.199999999999999956 ) ) ;
#52926=CYLINDRICAL_SURFACE ( 'NONE', #68969, 0.9999999999999991118 ) ;
#52934=AXIS2_PLACEMENT_3D ( 'NONE', #56997, #5501, #28398 ) ;
#52950=DIRECTION ( 'NONE',  ( 0.000000000000000000, 0.000000000000000000, 1.000000000000000000 ) ) ;
#53050=DIRECTION ( 'NONE',  ( 0.000000000000000000, 0.000000000000000000, 1.000000000000000000 ) ) ;
#53349=ORIENTED_EDGE ( 'NONE', *, *, #42854, .F. ) ;
#53438=CIRCLE ( 'NONE', #9050, 11.59999999999999964 ) ;
#53499=EDGE_CURVE ( 'NONE', #63816, #71661, #55890, .T. ) ;
#53522=AXIS2_PLACEMENT_3D ( 'NONE', #46081, #12953, #35891 ) ;
#53629=SHAPE_REPRESENTATION_RELATIONSHIP ( 'NONE' , 'NONE' ,  #10045, #72270 ) ;
#53754=CARTESIAN_POINT ( 'NONE',  ( 4.250000000000000000, -13.95926121303099343, -1.199999999999999956 ) ) ;
#53803=ORIENTED_EDGE ( 'NONE', *, *, #34875, .T. ) ;
#53893=AXIS2_PLACEMENT_3D ( 'NONE', #21536, #16276, #38099 ) ;
#53918=DIRECTION ( 'NONE',  ( 0.000000000000000000, 0.000000000000000000, 1.000000000000000000 ) ) ;
#54022=VERTEX_POINT ( 'NONE', #47895 ) ;
#54051=SURFACE_STYLE_USAGE ( .BOTH. , #31100 ) ;
#54172=CIRCLE ( 'NONE', #52934, 14.09999999999999964 ) ;
#54398=ORIENTED_EDGE ( 'NONE', *, *, #27583, .F. ) ;
#54424=LINE ( 'NONE', #1857, #25320 ) ;
#54546=ORIENTED_EDGE ( 'NONE', *, *, #57536, .T. ) ;
#54548=DIRECTION ( 'NONE',  ( -1.000000000000000000, 0.000000000000000000, 0.000000000000000000 ) ) ;
#54932=EDGE_CURVE ( 'NONE', #49170, #15332, #25419, .T. ) ;
#55077=CARTESIAN_POINT ( 'NONE',  ( 7.893099573151324044, -11.68370571044642503, -1.199999999999999956 ) ) ;
#55107=SURFACE_STYLE_USAGE ( .BOTH. , #47999 ) ;
#55147=VECTOR ( 'NONE', #5211, 1000.000000000000000 ) ;
#55349=DIRECTION ( 'NONE',  ( 0.000000000000000000, 0.000000000000000000, 1.000000000000000000 ) ) ;
#55542=EDGE_LOOP ( 'NONE', ( #17735, #60223, #4578, #21887 ) ) ;
#55597=DIRECTION ( 'NONE',  ( -1.000000000000000000, 0.000000000000000000, 0.000000000000000000 ) ) ;
#55753=ORIENTED_EDGE ( 'NONE', *, *, #7656, .F. ) ;
#55756=EDGE_CURVE ( 'NONE', #62740, #185, #59411, .T. ) ;
#55824=CIRCLE ( 'NONE', #11377, 0.9999999999999991118 ) ;
#55890=CIRCLE ( 'NONE', #28237, 1.000000000000000888 ) ;
#56011=VERTEX_POINT ( 'NONE', #56371 ) ;
#56082=EDGE_CURVE ( 'NONE', #14793, #14764, #45472, .T. ) ;
#56101=CARTESIAN_POINT ( 'NONE',  ( -6.509281303079589520, -14.89695620656361008, 0.000000000000000000 ) ) ;
#56141=DIRECTION ( 'NONE',  ( 0.000000000000000000, 0.000000000000000000, 1.000000000000000000 ) ) ;
#56371=CARTESIAN_POINT ( 'NONE',  ( -7.468086116107294004, -12.33868914344945189, 0.000000000000000000 ) ) ;
#56741=CARTESIAN_POINT ( 'NONE',  ( 4.250000000000000000, -13.95926121303099343, 0.000000000000000000 ) ) ;
#56750=DIRECTION ( 'NONE',  ( 0.1736481776669309418, 0.9848077530122080203, -0.000000000000000000 ) ) ;
#56921=CARTESIAN_POINT ( 'NONE',  ( 1.250000000000000444, -16.78109714094927085, -1.199999999999999956 ) ) ;
#56946=DIRECTION ( 'NONE',  ( -0.000000000000000000, -0.000000000000000000, -1.000000000000000000 ) ) ;
#56958=EDGE_CURVE ( 'NONE', #22660, #48200, #5343, .T. ) ;
#56997=CARTESIAN_POINT ( 'NONE',  ( 0.000000000000000000, 0.000000000000000000, -1.199999999999999956 ) ) ;
#57077=EDGE_CURVE ( 'NONE', #20209, #14859, #71415, .T. ) ;
#57079=CARTESIAN_POINT ( 'NONE',  ( -1.250000000000002442, -12.36245420541525242, 0.000000000000000000 ) ) ;
#57116=PLANE ( 'NONE',  #64437 ) ;
#57130=VECTOR ( 'NONE', #66696, 1000.000000000000000 ) ;
#57193=AXIS2_PLACEMENT_3D ( 'NONE', #34725, #1304, #68948 ) ;
#57401=ADVANCED_FACE ( 'NONE', ( #15225 ), #31767, .F. ) ;
#57465=ORIENTED_EDGE ( 'NONE', *, *, #52417, .T. ) ;
#57536=EDGE_CURVE ( 'NONE', #45615, #1516, #9213, .T. ) ;
#57649=DIRECTION ( 'NONE',  ( 0.1736481776669309696, -0.9848077530122080203, 0.000000000000000000 ) ) ;
#57785=CIRCLE ( 'NONE', #36207, 14.09999999999999964 ) ;
#58085=DIRECTION ( 'NONE',  ( 1.000000000000000000, 0.000000000000000000, 0.000000000000000000 ) ) ;
#58128=CARTESIAN_POINT ( 'NONE',  ( 0.000000000000000000, 0.000000000000000000, 0.000000000000000000 ) ) ;
#58296=CARTESIAN_POINT ( 'NONE',  ( -1.250000000000000000, -12.36245420541525597, 0.000000000000000000 ) ) ;
#58479=LINE ( 'NONE', #17519, #71497 ) ;
#58675=CARTESIAN_POINT ( 'NONE',  ( 6.719258119307966126, -15.35072898742050462, -1.199999999999999956 ) ) ;
#59211=DIRECTION ( 'NONE',  ( 1.000000000000000000, 0.000000000000000000, 0.000000000000000000 ) ) ;
#59255=DIRECTION ( 'NONE',  ( 1.000000000000000000, 0.000000000000000000, 0.000000000000000000 ) ) ;
#59377=VECTOR ( 'NONE', #37342, 1000.000000000000000 ) ;
#59411=LINE ( 'NONE', #58296, #68743 ) ;
#59561=CYLINDRICAL_SURFACE ( 'NONE', #25071, 11.59999999999999964 ) ;
#59730=ORIENTED_EDGE ( 'NONE', *, *, #3528, .F. ) ;
#59784=DIRECTION ( 'NONE',  ( 9.814797785686868941E-17, 1.000000000000000000, -0.000000000000000000 ) ) ;
#60002=AXIS2_PLACEMENT_3D ( 'NONE', #43408, #31716, #26080 ) ;
#60070=FACE_OUTER_BOUND ( 'NONE', #19579, .T. ) ;
#60107=CIRCLE ( 'NONE', #32501, 16.00000000000000000 ) ;
#60127=EDGE_CURVE ( 'NONE', #64091, #20620, #67919, .T. ) ;
#60223=ORIENTED_EDGE ( 'NONE', *, *, #67484, .F. ) ;
#60280=EDGE_CURVE ( 'NONE', #49170, #3025, #30986, .T. ) ;
#60561=CIRCLE ( 'NONE', #17296, 0.5000000000000004441 ) ;
#60702=DIRECTION ( 'NONE',  ( 0.000000000000000000, 0.000000000000000000, 1.000000000000000000 ) ) ;
#60810=DIRECTION ( 'NONE',  ( 1.000000000000000000, 0.000000000000000000, 0.000000000000000000 ) ) ;
#60887=CIRCLE ( 'NONE', #34467, 1.000000000000000000 ) ;
#61019=DIRECTION ( 'NONE',  ( 0.000000000000000000, 0.000000000000000000, 1.000000000000000000 ) ) ;
#61095=DIRECTION ( 'NONE',  ( 0.000000000000000000, 0.000000000000000000, 1.000000000000000000 ) ) ;
#61182=DIRECTION ( 'NONE',  ( 0.000000000000000000, 0.000000000000000000, 1.000000000000000000 ) ) ;
#61422=DIRECTION ( 'NONE',  ( 1.000000000000000000, 0.000000000000000000, 0.000000000000000000 ) ) ;
#61460=DIRECTION ( 'NONE',  ( 1.000000000000000000, 0.000000000000000000, 0.000000000000000000 ) ) ;
#61690=EDGE_LOOP ( 'NONE', ( #18017, #32407 ) ) ;
#61752=AXIS2_PLACEMENT_3D ( 'NONE', #44174, #61095, #32511 ) ;
#62288=LINE ( 'NONE', #67176, #69525 ) ;
#62458=DIRECTION ( 'NONE',  ( 0.000000000000000000, 0.000000000000000000, 1.000000000000000000 ) ) ;
#62601=ADVANCED_FACE ( 'NONE', ( #68720 ), #40883, .T. ) ;
#62740=VERTEX_POINT ( 'NONE', #13768 ) ;
#62789=AXIS2_PLACEMENT_3D ( 'NONE', #23808, #70023, #47483 ) ;
#62958=ADVANCED_FACE ( 'NONE', ( #52058, #601, #17846 ), #23138, .T. ) ;
#63044=DIRECTION ( 'NONE',  ( 0.000000000000000000, 0.000000000000000000, 1.000000000000000000 ) ) ;
#63083=DIRECTION ( 'NONE',  ( 1.000000000000000000, 0.000000000000000000, 0.000000000000000000 ) ) ;
#63156=ADVANCED_FACE ( 'NONE', ( #36615 ), #59561, .F. ) ;
#63180=EDGE_CURVE ( 'NONE', #14764, #45615, #20221, .T. ) ;
#63289=FACE_OUTER_BOUND ( 'NONE', #33096, .T. ) ;
#63426=ADVANCED_FACE ( 'NONE', ( #63289 ), #69653, .T. ) ;
#63584=PLANE ( 'NONE',  #15587 ) ;
#63707=FACE_BOUND ( 'NONE', #33466, .T. ) ;
#63719=VERTEX_POINT ( 'NONE', #23699 ) ;
#63816=VERTEX_POINT ( 'NONE', #23341 ) ;
#64021=EDGE_LOOP ( 'NONE', ( #33386, #14337, #31972, #4381 ) ) ;
#64091=VERTEX_POINT ( 'NONE', #64909 ) ;
#64122=CIRCLE ( 'NONE', #73693, 14.09999999999999964 ) ;
#64187=CARTESIAN_POINT ( 'NONE',  ( 0.000000000000000000, -0.8299999999999999600, -1.199999999999999956 ) ) ;
#64231=FACE_OUTER_BOUND ( 'NONE', #68553, .T. ) ;
#64280=ORIENTED_EDGE ( 'NONE', *, *, #71981, .T. ) ;
#64353=ORIENTED_EDGE ( 'NONE', *, *, #10532, .F. ) ;
#64437=AXIS2_PLACEMENT_3D ( 'NONE', #45846, #5620, #15 ) ;
#64469=CARTESIAN_POINT ( 'NONE',  ( -4.250000000000000000, -13.95926121303099343, -1.199999999999999956 ) ) ;
#64699=LINE ( 'NONE', #70680, #6183 ) ;
#64789=CARTESIAN_POINT ( 'NONE',  ( 1.250000000000000000, -12.36245420541525597, -1.199999999999999956 ) ) ;
#64909=CARTESIAN_POINT ( 'NONE',  ( 11.59999999999999964, -0.8299999999999999600, -1.199999999999999956 ) ) ;
#64956=FACE_OUTER_BOUND ( 'NONE', #6119, .T. ) ;
#65005=CIRCLE ( 'NONE', #73409, 11.59999999999999964 ) ;
#65095=EDGE_CURVE ( 'NONE', #63816, #15441, #68461, .T. ) ;
#65214=DIRECTION ( 'NONE',  ( 1.000000000000000000, 0.000000000000000000, 0.000000000000000000 ) ) ;
#65298=( NAMED_UNIT ( * ) SI_UNIT ( $, .STERADIAN. ) SOLID_ANGLE_UNIT ( ) );
#65353=CARTESIAN_POINT ( 'NONE',  ( 0.000000000000000000, -0.8299999999999999600, 0.000000000000000000 ) ) ;
#65457=AXIS2_PLACEMENT_3D ( 'NONE', #49136, #31469, #48032 ) ;
#65685=ORIENTED_EDGE ( 'NONE', *, *, #60280, .F. ) ;
#65701=( NAMED_UNIT ( * ) SI_UNIT ( $, .STERADIAN. ) SOLID_ANGLE_UNIT ( ) );
#65808=CARTESIAN_POINT ( 'NONE',  ( 0.000000000000000000, -0.8299999999999999600, 0.000000000000000000 ) ) ;
#65870=ORIENTED_EDGE ( 'NONE', *, *, #42673, .T. ) ;
#65882=DIRECTION ( 'NONE',  ( 0.1736481776669309696, 0.9848077530122080203, 0.000000000000000000 ) ) ;
#66135=ORIENTED_EDGE ( 'NONE', *, *, #43810, .T. ) ;
#66185=PRODUCT ( 'CIRCLIP DIN 471 - 25 \X2\00d7\X0\ 1.2_GB_CONNECTING_PIECE_RING_RRA 25', 'CIRCLIP DIN 471 - 25 \X2\00d7\X0\ 1.2_GB_CONNECTING_PIECE_RING_RRA 25', '', ( #27559 ) ) ;
#66289=DIRECTION ( 'NONE',  ( -1.000000000000000000, 0.000000000000000000, 0.000000000000000000 ) ) ;
#66303=ORIENTED_EDGE ( 'NONE', *, *, #10532, .T. ) ;
#66320=ADVANCED_FACE ( 'NONE', ( #14726 ), #25644, .T. ) ;
#66423=AXIS2_PLACEMENT_3D ( 'NONE', #17348, #5348, #34634 ) ;
#66594=ORIENTED_EDGE ( 'NONE', *, *, #52266, .F. ) ;
#66696=DIRECTION ( 'NONE',  ( 0.000000000000000000, 0.000000000000000000, 1.000000000000000000 ) ) ;
#66734=LINE ( 'NONE', #31765, #11286 ) ;
#66781=CARTESIAN_POINT ( 'NONE',  ( 1.250000000000000000, -12.36245420541525597, -1.199999999999999956 ) ) ;
#67021=CARTESIAN_POINT ( 'NONE',  ( -7.001685179585692254, -14.98378029539707512, -1.199999999999999956 ) ) ;
#67157=ORIENTED_EDGE ( 'NONE', *, *, #54932, .T. ) ;
#67176=CARTESIAN_POINT ( 'NONE',  ( -7.543218489614351263, -11.91259227951415056, -1.199999999999999956 ) ) ;
#67215=EDGE_CURVE ( 'NONE', #11203, #22660, #834, .T. ) ;
#67284=AXIS2_PLACEMENT_3D ( 'NONE', #69697, #47869, #13652 ) ;
#67373=ORIENTED_EDGE ( 'NONE', *, *, #41029, .T. ) ;
#67427=EDGE_LOOP ( 'NONE', ( #35448, #64353 ) ) ;
#67484=EDGE_CURVE ( 'NONE', #20620, #26097, #58479, .T. ) ;
#67602=CARTESIAN_POINT ( 'NONE',  ( 1.250000000000000000, -12.36245420541525597, 0.000000000000000000 ) ) ;
#67771=DIRECTION ( 'NONE',  ( 0.000000000000000000, 0.000000000000000000, 1.000000000000000000 ) ) ;
#67874=ORIENTED_EDGE ( 'NONE', *, *, #55756, .F. ) ;
#67919=CIRCLE ( 'NONE', #53522, 11.59999999999999964 ) ;
#68054=EDGE_CURVE ( 'NONE', #20087, #70347, #47578, .T. ) ;
#68209=CARTESIAN_POINT ( 'NONE',  ( 0.000000000000000000, 0.000000000000000000, 0.000000000000000000 ) ) ;
#68332=CARTESIAN_POINT ( 'NONE',  ( -5.250000000000000888, -13.95926121303099343, 0.000000000000000000 ) ) ;
#68422=VECTOR ( 'NONE', #39339, 1000.000000000000000 ) ;
#68461=LINE ( 'NONE', #72945, #23898 ) ;
#68553=EDGE_LOOP ( 'NONE', ( #54398, #15075, #66303, #31868 ) ) ;
#68614=CIRCLE ( 'NONE', #62789, 11.59999999999999964 ) ;
#68621=ORIENTED_EDGE ( 'NONE', *, *, #56958, .F. ) ;
#68711=DIRECTION ( 'NONE',  ( 0.000000000000000000, 0.000000000000000000, 1.000000000000000000 ) ) ;
#68720=FACE_OUTER_BOUND ( 'NONE', #12180, .T. ) ;
#68743=VECTOR ( 'NONE', #59784, 1000.000000000000000 ) ;
#68760=ADVANCED_FACE ( 'NONE', ( #17856 ), #35518, .F. ) ;
#68948=DIRECTION ( 'NONE',  ( -1.000000000000000000, 0.000000000000000000, 0.000000000000000000 ) ) ;
#68969=AXIS2_PLACEMENT_3D ( 'NONE', #1467, #42025, #24356 ) ;
#69525=VECTOR ( 'NONE', #44997, 1000.000000000000114 ) ;
#69653=PLANE ( 'NONE',  #1193 ) ;
#69697=CARTESIAN_POINT ( 'NONE',  ( 0.000000000000000000, -0.8299999999999999600, 0.000000000000000000 ) ) ;
#69722=DIRECTION ( 'NONE',  ( -0.000000000000000000, 0.000000000000000000, -1.000000000000000000 ) ) ;
#69846=( NAMED_UNIT ( * ) PLANE_ANGLE_UNIT ( ) SI_UNIT ( $, .RADIAN. ) );
#70007=DIRECTION ( 'NONE',  ( -0.9848077530122080203, -0.1736481776669309696, 0.000000000000000000 ) ) ;
#70023=DIRECTION ( 'NONE',  ( -0.000000000000000000, -0.000000000000000000, -1.000000000000000000 ) ) ;
#70264=EDGE_LOOP ( 'NONE', ( #18839, #2462, #50792, #36987 ) ) ;
#70347=VERTEX_POINT ( 'NONE', #37708 ) ;
#70408=CIRCLE ( 'NONE', #38014, 0.5000000000000004441 ) ;
#70508=AXIS2_PLACEMENT_3D ( 'NONE', #56741, #29888, #22141 ) ;
#70550=DIRECTION ( 'NONE',  ( 0.000000000000000000, 0.000000000000000000, 1.000000000000000000 ) ) ;
#70680=CARTESIAN_POINT ( 'NONE',  ( -1.250000000000002442, -12.36245420541525242, -1.199999999999999956 ) ) ;
#70752=CARTESIAN_POINT ( 'NONE',  ( -1.250000000000002442, -12.36245420541525242, -1.199999999999999956 ) ) ;
#70837=VERTEX_POINT ( 'NONE', #16910 ) ;
#70956=CYLINDRICAL_SURFACE ( 'NONE', #21351, 0.5000000000000004441 ) ;
#71232=DIRECTION ( 'NONE',  ( 0.000000000000000000, 0.000000000000000000, 1.000000000000000000 ) ) ;
#71392=CARTESIAN_POINT ( 'NONE',  ( 7.468086116107294004, -12.33868914344945189, -1.199999999999999956 ) ) ;
#71415=LINE ( 'NONE', #58675, #22085 ) ;
#71485=CARTESIAN_POINT ( 'NONE',  ( 0.000000000000000000, -0.8299999999999999600, -1.199999999999999956 ) ) ;
#71491=DIRECTION ( 'NONE',  ( 0.9848077530122080203, -0.1736481776669309696, 0.000000000000000000 ) ) ;
#71497=VECTOR ( 'NONE', #63044, 1000.000000000000000 ) ;
#71531=ADVANCED_FACE ( 'NONE', ( #39625 ), #63584, .T. ) ;
#71649=PRESENTATION_STYLE_ASSIGNMENT (( #55107 ) ) ;
#71661=VERTEX_POINT ( 'NONE', #50892 ) ;
#71678=DIRECTION ( 'NONE',  ( 1.000000000000000000, 0.000000000000000000, 0.000000000000000000 ) ) ;
#71912=CIRCLE ( 'NONE', #10700, 16.00000000000000000 ) ;
#71981=EDGE_CURVE ( 'NONE', #22641, #15441, #43246, .T. ) ;
#72011=CARTESIAN_POINT ( 'NONE',  ( 7.001685179585692254, -14.98378029539707512, -1.199999999999999956 ) ) ;
#72170=ORIENTED_EDGE ( 'NONE', *, *, #22835, .T. ) ;
#72270=ADVANCED_BREP_SHAPE_REPRESENTATION ( '', ( #12168, #43395 ), #32718 ) ;
#72304=EDGE_LOOP ( 'NONE', ( #13410, #15141, #28101, #18247 ) ) ;
#72424=DIRECTION ( 'NONE',  ( -0.000000000000000000, -0.000000000000000000, 1.000000000000000000 ) ) ;
#72505=VERTEX_POINT ( 'NONE', #2190 ) ;
#72550=ORIENTED_EDGE ( 'NONE', *, *, #42673, .F. ) ;
#72656=ORIENTED_EDGE ( 'NONE', *, *, #29030, .T. ) ;
#72798=CARTESIAN_POINT ( 'NONE',  ( 6.509281303079589520, -14.89695620656361008, -1.199999999999999956 ) ) ;
#72805=CLOSED_SHELL ( 'NONE', ( #8900, #50563, #26284, #29103, #63156, #32860, #5995, #6331, #57401, #71531, #62601, #63426, #46180, #66320, #62958, #34714, #68760, #11105, #48782, #29414, #7500, #47676 ) ) ;
#72945=CARTESIAN_POINT ( 'NONE',  ( -5.250000000000000888, -13.95926121303099343, -1.199999999999999956 ) ) ;
#73174=VECTOR ( 'NONE', #70550, 1000.000000000000000 ) ;
#73335=ORIENTED_EDGE ( 'NONE', *, *, #35627, .F. ) ;
#73409=AXIS2_PLACEMENT_3D ( 'NONE', #71485, #14357, #37308 ) ;
#73693=AXIS2_PLACEMENT_3D ( 'NONE', #68209, #9577, #50906 ) ;
#74124=DIRECTION ( 'NONE',  ( 0.1736481776669309418, 0.9848077530122080203, -0.000000000000000000 ) ) ;
#74206=CARTESIAN_POINT ( 'NONE',  ( 0.000000000000000000, -0.8299999999999999600, -1.199999999999999956 ) ) ;
#74239=ORIENTED_EDGE ( 'NONE', *, *, #65095, .F. ) ;
ENDSEC;
END-ISO-10303-21;
